ISO-10303-21;
HEADER;
/* Generated by software containing ST-Developer
 * from STEP Tools, Inc. (www.steptools.com) 
 */

FILE_DESCRIPTION(
/* description */ (''),
/* implementation_level */ '2;1');

FILE_NAME(
/* name */ '03_Ball_Bearing_MR106ZZ_6x10x3.step',
/* time_stamp */ '2026-10-25T01:35:35-07:00',
/* author */ (''),
/* organization */ (''),
/* preprocessor_version */ 'ST-DEVELOPER v20.2',
/* originating_system */ 'Autodesk Translation Framework v15.15.0.0',
/* authorisation */ '');

FILE_SCHEMA (('AUTOMOTIVE_DESIGN { 1 0 10303 214 3 1 1 }'));
ENDSEC;

DATA;
#10=MECHANICAL_DESIGN_GEOMETRIC_PRESENTATION_REPRESENTATION('',(#262),#11430);
#238=SHAPE_REPRESENTATION_RELATIONSHIP('SRR','None',#11481,#250);
#250=ADVANCED_BREP_SHAPE_REPRESENTATION('',(#274),#11420);
#262=STYLED_ITEM('',(#11609),#274);
#274=MANIFOLD_SOLID_BREP('Body1',#4463);
#292=FACE_BOUND('',#854,.T.);
#293=FACE_BOUND('',#857,.T.);
#294=FACE_BOUND('',#862,.T.);
#295=FACE_BOUND('',#865,.T.);
#296=FACE_BOUND('',#868,.T.);
#297=FACE_BOUND('',#873,.T.);
#345=PLANE('',#4704);
#346=PLANE('',#4708);
#347=PLANE('',#4716);
#348=PLANE('',#4720);
#349=PLANE('',#4724);
#350=PLANE('',#4732);
#443=CYLINDRICAL_SURFACE('',#4712,5.);
#444=CYLINDRICAL_SURFACE('',#4728,3.);
#576=FACE_OUTER_BOUND('',#852,.T.);
#577=FACE_OUTER_BOUND('',#853,.T.);
#578=FACE_OUTER_BOUND('',#855,.T.);
#579=FACE_OUTER_BOUND('',#856,.T.);
#580=FACE_OUTER_BOUND('',#858,.T.);
#581=FACE_OUTER_BOUND('',#859,.T.);
#582=FACE_OUTER_BOUND('',#860,.T.);
#583=FACE_OUTER_BOUND('',#861,.T.);
#584=FACE_OUTER_BOUND('',#863,.T.);
#585=FACE_OUTER_BOUND('',#864,.T.);
#586=FACE_OUTER_BOUND('',#866,.T.);
#587=FACE_OUTER_BOUND('',#867,.T.);
#588=FACE_OUTER_BOUND('',#869,.T.);
#589=FACE_OUTER_BOUND('',#870,.T.);
#590=FACE_OUTER_BOUND('',#871,.T.);
#591=FACE_OUTER_BOUND('',#872,.T.);
#852=EDGE_LOOP('',(#3083,#3084,#3085,#3086));
#853=EDGE_LOOP('',(#3087));
#854=EDGE_LOOP('',(#3088));
#855=EDGE_LOOP('',(#3089,#3090,#3091,#3092));
#856=EDGE_LOOP('',(#3093));
#857=EDGE_LOOP('',(#3094));
#858=EDGE_LOOP('',(#3095,#3096,#3097,#3098));
#859=EDGE_LOOP('',(#3099,#3100,#3101,#3102));
#860=EDGE_LOOP('',(#3103,#3104,#3105,#3106));
#861=EDGE_LOOP('',(#3107));
#862=EDGE_LOOP('',(#3108));
#863=EDGE_LOOP('',(#3109,#3110,#3111,#3112));
#864=EDGE_LOOP('',(#3113));
#865=EDGE_LOOP('',(#3114));
#866=EDGE_LOOP('',(#3115,#3116,#3117,#3118));
#867=EDGE_LOOP('',(#3119));
#868=EDGE_LOOP('',(#3120));
#869=EDGE_LOOP('',(#3121,#3122,#3123,#3124));
#870=EDGE_LOOP('',(#3125,#3126,#3127,#3128));
#871=EDGE_LOOP('',(#3129,#3130,#3131,#3132));
#872=EDGE_LOOP('',(#3133));
#873=EDGE_LOOP('',(#3134));
#1159=LINE('',#6541,#1449);
#1160=LINE('',#6548,#1450);
#1161=LINE('',#6556,#1451);
#1162=LINE('',#6560,#1452);
#1163=LINE('',#6564,#1453);
#1164=LINE('',#6570,#1454);
#1165=LINE('',#6578,#1455);
#1166=LINE('',#6584,#1456);
#1167=LINE('',#6588,#1457);
#1168=LINE('',#6592,#1458);
#1449=VECTOR('',#5335,3.825);
#1450=VECTOR('',#5344,4.275);
#1451=VECTOR('',#5355,4.925);
#1452=VECTOR('',#5360,5.);
#1453=VECTOR('',#5365,4.925);
#1454=VECTOR('',#5372,4.275);
#1455=VECTOR('',#5383,3.825);
#1456=VECTOR('',#5390,3.075);
#1457=VECTOR('',#5395,3.);
#1458=VECTOR('',#5400,3.075);
#1722=CIRCLE('',#4702,3.85);
#1723=CIRCLE('',#4703,3.8);
#1724=CIRCLE('',#4705,4.25);
#1725=CIRCLE('',#4707,4.3);
#1726=CIRCLE('',#4709,4.85);
#1727=CIRCLE('',#4711,5.);
#1728=CIRCLE('',#4713,5.);
#1729=CIRCLE('',#4715,4.85);
#1730=CIRCLE('',#4717,4.3);
#1731=CIRCLE('',#4719,4.25);
#1732=CIRCLE('',#4721,3.85);
#1733=CIRCLE('',#4723,3.8);
#1734=CIRCLE('',#4725,3.15);
#1735=CIRCLE('',#4727,3.);
#1736=CIRCLE('',#4729,3.);
#1737=CIRCLE('',#4731,3.15);
#1923=VERTEX_POINT('',#6538);
#1924=VERTEX_POINT('',#6540);
#1925=VERTEX_POINT('',#6544);
#1926=VERTEX_POINT('',#6547);
#1927=VERTEX_POINT('',#6551);
#1928=VERTEX_POINT('',#6554);
#1929=VERTEX_POINT('',#6558);
#1930=VERTEX_POINT('',#6562);
#1931=VERTEX_POINT('',#6566);
#1932=VERTEX_POINT('',#6569);
#1933=VERTEX_POINT('',#6573);
#1934=VERTEX_POINT('',#6576);
#1935=VERTEX_POINT('',#6580);
#1936=VERTEX_POINT('',#6583);
#1937=VERTEX_POINT('',#6587);
#1938=VERTEX_POINT('',#6591);
#2359=EDGE_CURVE('',#1923,#1923,#1722,.T.);
#2360=EDGE_CURVE('',#1923,#1924,#1159,.T.);
#2361=EDGE_CURVE('',#1924,#1924,#1723,.T.);
#2362=EDGE_CURVE('',#1925,#1925,#1724,.T.);
#2363=EDGE_CURVE('',#1925,#1926,#1160,.T.);
#2364=EDGE_CURVE('',#1926,#1926,#1725,.T.);
#2365=EDGE_CURVE('',#1927,#1927,#1726,.T.);
#2366=EDGE_CURVE('',#1928,#1928,#1727,.T.);
#2367=EDGE_CURVE('',#1928,#1927,#1161,.T.);
#2368=EDGE_CURVE('',#1929,#1929,#1728,.T.);
#2369=EDGE_CURVE('',#1929,#1928,#1162,.T.);
#2370=EDGE_CURVE('',#1930,#1930,#1729,.T.);
#2371=EDGE_CURVE('',#1930,#1929,#1163,.T.);
#2372=EDGE_CURVE('',#1931,#1931,#1730,.T.);
#2373=EDGE_CURVE('',#1931,#1932,#1164,.T.);
#2374=EDGE_CURVE('',#1932,#1932,#1731,.T.);
#2375=EDGE_CURVE('',#1933,#1933,#1732,.T.);
#2376=EDGE_CURVE('',#1934,#1934,#1733,.T.);
#2377=EDGE_CURVE('',#1934,#1933,#1165,.T.);
#2378=EDGE_CURVE('',#1935,#1935,#1734,.T.);
#2379=EDGE_CURVE('',#1935,#1936,#1166,.T.);
#2380=EDGE_CURVE('',#1936,#1936,#1735,.T.);
#2381=EDGE_CURVE('',#1936,#1937,#1167,.T.);
#2382=EDGE_CURVE('',#1937,#1937,#1736,.T.);
#2383=EDGE_CURVE('',#1937,#1938,#1168,.T.);
#2384=EDGE_CURVE('',#1938,#1938,#1737,.T.);
#3083=ORIENTED_EDGE('',*,*,#2359,.F.);
#3084=ORIENTED_EDGE('',*,*,#2360,.T.);
#3085=ORIENTED_EDGE('',*,*,#2361,.T.);
#3086=ORIENTED_EDGE('',*,*,#2360,.F.);
#3087=ORIENTED_EDGE('',*,*,#2362,.F.);
#3088=ORIENTED_EDGE('',*,*,#2359,.T.);
#3089=ORIENTED_EDGE('',*,*,#2362,.T.);
#3090=ORIENTED_EDGE('',*,*,#2363,.T.);
#3091=ORIENTED_EDGE('',*,*,#2364,.F.);
#3092=ORIENTED_EDGE('',*,*,#2363,.F.);
#3093=ORIENTED_EDGE('',*,*,#2365,.F.);
#3094=ORIENTED_EDGE('',*,*,#2364,.T.);
#3095=ORIENTED_EDGE('',*,*,#2366,.F.);
#3096=ORIENTED_EDGE('',*,*,#2367,.T.);
#3097=ORIENTED_EDGE('',*,*,#2365,.T.);
#3098=ORIENTED_EDGE('',*,*,#2367,.F.);
#3099=ORIENTED_EDGE('',*,*,#2368,.F.);
#3100=ORIENTED_EDGE('',*,*,#2369,.T.);
#3101=ORIENTED_EDGE('',*,*,#2366,.T.);
#3102=ORIENTED_EDGE('',*,*,#2369,.F.);
#3103=ORIENTED_EDGE('',*,*,#2370,.F.);
#3104=ORIENTED_EDGE('',*,*,#2371,.T.);
#3105=ORIENTED_EDGE('',*,*,#2368,.T.);
#3106=ORIENTED_EDGE('',*,*,#2371,.F.);
#3107=ORIENTED_EDGE('',*,*,#2370,.T.);
#3108=ORIENTED_EDGE('',*,*,#2372,.F.);
#3109=ORIENTED_EDGE('',*,*,#2372,.T.);
#3110=ORIENTED_EDGE('',*,*,#2373,.T.);
#3111=ORIENTED_EDGE('',*,*,#2374,.F.);
#3112=ORIENTED_EDGE('',*,*,#2373,.F.);
#3113=ORIENTED_EDGE('',*,*,#2374,.T.);
#3114=ORIENTED_EDGE('',*,*,#2375,.F.);
#3115=ORIENTED_EDGE('',*,*,#2376,.F.);
#3116=ORIENTED_EDGE('',*,*,#2377,.T.);
#3117=ORIENTED_EDGE('',*,*,#2375,.T.);
#3118=ORIENTED_EDGE('',*,*,#2377,.F.);
#3119=ORIENTED_EDGE('',*,*,#2376,.T.);
#3120=ORIENTED_EDGE('',*,*,#2378,.F.);
#3121=ORIENTED_EDGE('',*,*,#2378,.T.);
#3122=ORIENTED_EDGE('',*,*,#2379,.T.);
#3123=ORIENTED_EDGE('',*,*,#2380,.F.);
#3124=ORIENTED_EDGE('',*,*,#2379,.F.);
#3125=ORIENTED_EDGE('',*,*,#2380,.T.);
#3126=ORIENTED_EDGE('',*,*,#2381,.T.);
#3127=ORIENTED_EDGE('',*,*,#2382,.F.);
#3128=ORIENTED_EDGE('',*,*,#2381,.F.);
#3129=ORIENTED_EDGE('',*,*,#2382,.T.);
#3130=ORIENTED_EDGE('',*,*,#2383,.T.);
#3131=ORIENTED_EDGE('',*,*,#2384,.F.);
#3132=ORIENTED_EDGE('',*,*,#2383,.F.);
#3133=ORIENTED_EDGE('',*,*,#2361,.F.);
#3134=ORIENTED_EDGE('',*,*,#2384,.T.);
#4151=CONICAL_SURFACE('',#4701,3.825,0.244978663126864);
#4152=CONICAL_SURFACE('',#4706,4.275,0.244978663126864);
#4153=CONICAL_SURFACE('',#4710,4.925,0.785398163397449);
#4154=CONICAL_SURFACE('',#4714,4.925,0.78539816339745);
#4155=CONICAL_SURFACE('',#4718,4.275,0.244978663126864);
#4156=CONICAL_SURFACE('',#4722,3.825,0.244978663126864);
#4157=CONICAL_SURFACE('',#4726,3.075,0.78539816339745);
#4158=CONICAL_SURFACE('',#4730,3.075,0.785398163397449);
#4243=ADVANCED_FACE('',(#576),#4151,.T.);
#4244=ADVANCED_FACE('',(#577,#292),#345,.T.);
#4245=ADVANCED_FACE('',(#578),#4152,.F.);
#4246=ADVANCED_FACE('',(#579,#293),#346,.T.);
#4247=ADVANCED_FACE('',(#580),#4153,.T.);
#4248=ADVANCED_FACE('',(#581),#443,.T.);
#4249=ADVANCED_FACE('',(#582),#4154,.T.);
#4250=ADVANCED_FACE('',(#583,#294),#347,.T.);
#4251=ADVANCED_FACE('',(#584),#4155,.F.);
#4252=ADVANCED_FACE('',(#585,#295),#348,.T.);
#4253=ADVANCED_FACE('',(#586),#4156,.T.);
#4254=ADVANCED_FACE('',(#587,#296),#349,.T.);
#4255=ADVANCED_FACE('',(#588),#4157,.F.);
#4256=ADVANCED_FACE('',(#589),#444,.F.);
#4257=ADVANCED_FACE('',(#590),#4158,.F.);
#4258=ADVANCED_FACE('',(#591,#297),#350,.T.);
#4463=CLOSED_SHELL('',(#4243,#4244,#4245,#4246,#4247,#4248,#4249,#4250,
#4251,#4252,#4253,#4254,#4255,#4256,#4257,#4258));
#4700=AXIS2_PLACEMENT_3D('',#6536,#5329,#5330);
#4701=AXIS2_PLACEMENT_3D('',#6537,#5331,#5332);
#4702=AXIS2_PLACEMENT_3D('',#6539,#5333,#5334);
#4703=AXIS2_PLACEMENT_3D('',#6542,#5336,#5337);
#4704=AXIS2_PLACEMENT_3D('',#6543,#5338,#5339);
#4705=AXIS2_PLACEMENT_3D('',#6545,#5340,#5341);
#4706=AXIS2_PLACEMENT_3D('',#6546,#5342,#5343);
#4707=AXIS2_PLACEMENT_3D('',#6549,#5345,#5346);
#4708=AXIS2_PLACEMENT_3D('',#6550,#5347,#5348);
#4709=AXIS2_PLACEMENT_3D('',#6552,#5349,#5350);
#4710=AXIS2_PLACEMENT_3D('',#6553,#5351,#5352);
#4711=AXIS2_PLACEMENT_3D('',#6555,#5353,#5354);
#4712=AXIS2_PLACEMENT_3D('',#6557,#5356,#5357);
#4713=AXIS2_PLACEMENT_3D('',#6559,#5358,#5359);
#4714=AXIS2_PLACEMENT_3D('',#6561,#5361,#5362);
#4715=AXIS2_PLACEMENT_3D('',#6563,#5363,#5364);
#4716=AXIS2_PLACEMENT_3D('',#6565,#5366,#5367);
#4717=AXIS2_PLACEMENT_3D('',#6567,#5368,#5369);
#4718=AXIS2_PLACEMENT_3D('',#6568,#5370,#5371);
#4719=AXIS2_PLACEMENT_3D('',#6571,#5373,#5374);
#4720=AXIS2_PLACEMENT_3D('',#6572,#5375,#5376);
#4721=AXIS2_PLACEMENT_3D('',#6574,#5377,#5378);
#4722=AXIS2_PLACEMENT_3D('',#6575,#5379,#5380);
#4723=AXIS2_PLACEMENT_3D('',#6577,#5381,#5382);
#4724=AXIS2_PLACEMENT_3D('',#6579,#5384,#5385);
#4725=AXIS2_PLACEMENT_3D('',#6581,#5386,#5387);
#4726=AXIS2_PLACEMENT_3D('',#6582,#5388,#5389);
#4727=AXIS2_PLACEMENT_3D('',#6585,#5391,#5392);
#4728=AXIS2_PLACEMENT_3D('',#6586,#5393,#5394);
#4729=AXIS2_PLACEMENT_3D('',#6589,#5396,#5397);
#4730=AXIS2_PLACEMENT_3D('',#6590,#5398,#5399);
#4731=AXIS2_PLACEMENT_3D('',#6593,#5401,#5402);
#4732=AXIS2_PLACEMENT_3D('',#6594,#5403,#5404);
#5329=DIRECTION('axis',(0.,0.,1.));
#5330=DIRECTION('refdir',(1.,0.,0.));
#5331=DIRECTION('center_axis',(1.,0.,0.));
#5332=DIRECTION('ref_axis',(0.,1.,0.));
#5333=DIRECTION('center_axis',(1.,0.,0.));
#5334=DIRECTION('ref_axis',(0.,0.,-1.));
#5335=DIRECTION('',(-0.970142500145332,0.242535625036333,2.97020476879948E-17));
#5336=DIRECTION('center_axis',(1.,0.,0.));
#5337=DIRECTION('ref_axis',(0.,0.,-1.));
#5338=DIRECTION('center_axis',(-1.,0.,0.));
#5339=DIRECTION('ref_axis',(0.,0.,1.));
#5340=DIRECTION('center_axis',(1.,0.,0.));
#5341=DIRECTION('ref_axis',(0.,0.,-1.));
#5342=DIRECTION('center_axis',(-1.,0.,0.));
#5343=DIRECTION('ref_axis',(0.,1.,0.));
#5344=DIRECTION('',(-0.970142500145332,-0.242535625036333,-2.97020476879948E-17));
#5345=DIRECTION('center_axis',(1.,0.,0.));
#5346=DIRECTION('ref_axis',(0.,0.,-1.));
#5347=DIRECTION('center_axis',(-1.,0.,0.));
#5348=DIRECTION('ref_axis',(0.,0.,1.));
#5349=DIRECTION('center_axis',(1.,0.,0.));
#5350=DIRECTION('ref_axis',(0.,0.,-1.));
#5351=DIRECTION('center_axis',(1.,0.,0.));
#5352=DIRECTION('ref_axis',(0.,1.,0.));
#5353=DIRECTION('center_axis',(1.,0.,0.));
#5354=DIRECTION('ref_axis',(0.,0.,-1.));
#5355=DIRECTION('',(-0.707106781186547,0.707106781186548,8.65956056235494E-17));
#5356=DIRECTION('center_axis',(1.,0.,0.));
#5357=DIRECTION('ref_axis',(0.,1.,0.));
#5358=DIRECTION('center_axis',(1.,0.,0.));
#5359=DIRECTION('ref_axis',(0.,0.,-1.));
#5360=DIRECTION('',(-1.,0.,0.));
#5361=DIRECTION('center_axis',(-1.,0.,0.));
#5362=DIRECTION('ref_axis',(0.,1.,0.));
#5363=DIRECTION('center_axis',(1.,0.,0.));
#5364=DIRECTION('ref_axis',(0.,0.,-1.));
#5365=DIRECTION('',(-0.707106781186546,-0.707106781186549,-8.65956056235495E-17));
#5366=DIRECTION('center_axis',(1.,0.,0.));
#5367=DIRECTION('ref_axis',(0.,0.,-1.));
#5368=DIRECTION('center_axis',(1.,0.,0.));
#5369=DIRECTION('ref_axis',(0.,0.,-1.));
#5370=DIRECTION('center_axis',(1.,0.,0.));
#5371=DIRECTION('ref_axis',(0.,1.,0.));
#5372=DIRECTION('',(-0.970142500145332,0.242535625036333,2.97020476879948E-17));
#5373=DIRECTION('center_axis',(1.,0.,0.));
#5374=DIRECTION('ref_axis',(0.,0.,-1.));
#5375=DIRECTION('center_axis',(1.,0.,0.));
#5376=DIRECTION('ref_axis',(0.,0.,-1.));
#5377=DIRECTION('center_axis',(1.,0.,0.));
#5378=DIRECTION('ref_axis',(0.,0.,-1.));
#5379=DIRECTION('center_axis',(-1.,0.,0.));
#5380=DIRECTION('ref_axis',(0.,1.,0.));
#5381=DIRECTION('center_axis',(1.,0.,0.));
#5382=DIRECTION('ref_axis',(0.,0.,-1.));
#5383=DIRECTION('',(-0.970142500145332,-0.242535625036333,-2.97020476879948E-17));
#5384=DIRECTION('center_axis',(1.,0.,0.));
#5385=DIRECTION('ref_axis',(0.,0.,-1.));
#5386=DIRECTION('center_axis',(1.,0.,0.));
#5387=DIRECTION('ref_axis',(0.,0.,-1.));
#5388=DIRECTION('center_axis',(1.,0.,0.));
#5389=DIRECTION('ref_axis',(0.,1.,0.));
#5390=DIRECTION('',(-0.707106781186546,0.707106781186549,8.65956056235495E-17));
#5391=DIRECTION('center_axis',(1.,0.,0.));
#5392=DIRECTION('ref_axis',(0.,0.,-1.));
#5393=DIRECTION('center_axis',(1.,0.,0.));
#5394=DIRECTION('ref_axis',(0.,1.,0.));
#5395=DIRECTION('',(-1.,0.,0.));
#5396=DIRECTION('center_axis',(1.,0.,0.));
#5397=DIRECTION('ref_axis',(0.,0.,-1.));
#5398=DIRECTION('center_axis',(-1.,0.,0.));
#5399=DIRECTION('ref_axis',(0.,1.,0.));
#5400=DIRECTION('',(-0.707106781186547,-0.707106781186548,-8.65956056235494E-17));
#5401=DIRECTION('center_axis',(1.,0.,0.));
#5402=DIRECTION('ref_axis',(0.,0.,-1.));
#5403=DIRECTION('center_axis',(-1.,0.,0.));
#5404=DIRECTION('ref_axis',(0.,0.,1.));
#6536=CARTESIAN_POINT('',(0.,0.,0.));
#6537=CARTESIAN_POINT('Origin',(0.1,0.,0.));
#6538=CARTESIAN_POINT('',(0.2,-3.85,-4.71489017671731E-16));
#6539=CARTESIAN_POINT('Origin',(0.2,0.,0.));
#6540=CARTESIAN_POINT('',(-3.46944695195361E-17,-3.8,-4.65365783675994E-16));
#6541=CARTESIAN_POINT('',(0.1,-3.825,-4.68427400673863E-16));
#6542=CARTESIAN_POINT('Origin',(0.,0.,0.));
#6543=CARTESIAN_POINT('Origin',(0.2,4.25,0.));
#6544=CARTESIAN_POINT('',(0.2,-4.25,-5.20474889637625E-16));
#6545=CARTESIAN_POINT('Origin',(0.2,0.,0.));
#6546=CARTESIAN_POINT('Origin',(0.1,0.,0.));
#6547=CARTESIAN_POINT('',(-5.20417042793042E-17,-4.3,-5.26598123633362E-16));
#6548=CARTESIAN_POINT('',(0.1,-4.275,-5.23536506635494E-16));
#6549=CARTESIAN_POINT('Origin',(0.,0.,0.));
#6550=CARTESIAN_POINT('Origin',(0.,4.85,0.));
#6551=CARTESIAN_POINT('',(-1.64798730217797E-16,-4.85,-5.93953697586466E-16));
#6552=CARTESIAN_POINT('Origin',(0.,0.,0.));
#6553=CARTESIAN_POINT('Origin',(0.075,0.,0.));
#6554=CARTESIAN_POINT('',(0.15,-5.,-6.12323399573677E-16));
#6555=CARTESIAN_POINT('Origin',(0.15,0.,0.));
#6556=CARTESIAN_POINT('',(0.075,-4.925,-6.03138548580071E-16));
#6557=CARTESIAN_POINT('Origin',(1.5,0.,0.));
#6558=CARTESIAN_POINT('',(2.85,-5.,-6.12323399573677E-16));
#6559=CARTESIAN_POINT('Origin',(2.85,0.,0.));
#6560=CARTESIAN_POINT('',(1.5,-5.,-6.12323399573677E-16));
#6561=CARTESIAN_POINT('Origin',(2.925,0.,0.));
#6562=CARTESIAN_POINT('',(3.,-4.85,-5.93953697586466E-16));
#6563=CARTESIAN_POINT('Origin',(3.,0.,0.));
#6564=CARTESIAN_POINT('',(2.925,-4.925,-6.03138548580071E-16));
#6565=CARTESIAN_POINT('Origin',(3.,4.3,0.));
#6566=CARTESIAN_POINT('',(3.,-4.3,-5.26598123633362E-16));
#6567=CARTESIAN_POINT('Origin',(3.,0.,0.));
#6568=CARTESIAN_POINT('Origin',(2.9,0.,0.));
#6569=CARTESIAN_POINT('',(2.8,-4.25,-5.20474889637625E-16));
#6570=CARTESIAN_POINT('',(2.9,-4.275,-5.23536506635494E-16));
#6571=CARTESIAN_POINT('Origin',(2.8,0.,0.));
#6572=CARTESIAN_POINT('Origin',(2.8,3.85,0.));
#6573=CARTESIAN_POINT('',(2.8,-3.85,-4.71489017671731E-16));
#6574=CARTESIAN_POINT('Origin',(2.8,0.,0.));
#6575=CARTESIAN_POINT('Origin',(2.9,0.,0.));
#6576=CARTESIAN_POINT('',(3.,-3.8,-4.65365783675994E-16));
#6577=CARTESIAN_POINT('Origin',(3.,0.,0.));
#6578=CARTESIAN_POINT('',(2.9,-3.825,-4.68427400673863E-16));
#6579=CARTESIAN_POINT('Origin',(3.,3.15,0.));
#6580=CARTESIAN_POINT('',(3.,-3.15,-3.85763741731416E-16));
#6581=CARTESIAN_POINT('Origin',(3.,0.,0.));
#6582=CARTESIAN_POINT('Origin',(2.925,0.,0.));
#6583=CARTESIAN_POINT('',(2.85,-3.,-3.67394039744206E-16));
#6584=CARTESIAN_POINT('',(2.925,-3.075,-3.76578890737811E-16));
#6585=CARTESIAN_POINT('Origin',(2.85,0.,0.));
#6586=CARTESIAN_POINT('Origin',(1.5,0.,0.));
#6587=CARTESIAN_POINT('',(0.15,-3.,-3.67394039744206E-16));
#6588=CARTESIAN_POINT('',(1.5,-3.,-3.67394039744206E-16));
#6589=CARTESIAN_POINT('Origin',(0.15,0.,0.));
#6590=CARTESIAN_POINT('Origin',(0.075,0.,0.));
#6591=CARTESIAN_POINT('',(-3.46944695195361E-17,-3.15,-3.85763741731416E-16));
#6592=CARTESIAN_POINT('',(0.075,-3.075,-3.76578890737811E-16));
#6593=CARTESIAN_POINT('Origin',(0.,0.,0.));
#6594=CARTESIAN_POINT('Origin',(0.,3.8,0.));
#11406=UNCERTAINTY_MEASURE_WITH_UNIT(LENGTH_MEASURE(0.01),#11431,
'DISTANCE_ACCURACY_VALUE',
'Maximum model space distance between geometric entities at asserted c
onnectivities');
#11416=UNCERTAINTY_MEASURE_WITH_UNIT(LENGTH_MEASURE(0.01),#11431,
'DISTANCE_ACCURACY_VALUE',
'Maximum model space distance between geometric entities at asserted c
onnectivities');
#11420=(
GEOMETRIC_REPRESENTATION_CONTEXT(3)
GLOBAL_UNCERTAINTY_ASSIGNED_CONTEXT((#11406))
GLOBAL_UNIT_ASSIGNED_CONTEXT((#11431,#11433,#11434))
REPRESENTATION_CONTEXT('','3D')
);
#11430=(
GEOMETRIC_REPRESENTATION_CONTEXT(3)
GLOBAL_UNCERTAINTY_ASSIGNED_CONTEXT((#11416))
GLOBAL_UNIT_ASSIGNED_CONTEXT((#11431,#11433,#11434))
REPRESENTATION_CONTEXT('','3D')
);
#11431=(
LENGTH_UNIT()
NAMED_UNIT(*)
SI_UNIT(.MILLI.,.METRE.)
);
#11433=(
NAMED_UNIT(*)
PLANE_ANGLE_UNIT()
SI_UNIT($,.RADIAN.)
);
#11434=(
NAMED_UNIT(*)
SI_UNIT($,.STERADIAN.)
SOLID_ANGLE_UNIT()
);
#11438=SHAPE_DEFINITION_REPRESENTATION(#11451,#11481);
#11451=PRODUCT_DEFINITION_SHAPE('',$,#11495);
#11481=SHAPE_REPRESENTATION('',(#4700),#11420);
#11491=PRODUCT_DEFINITION_CONTEXT('part definition',#11532,'design');
#11495=PRODUCT_DEFINITION('2026-10-25-00-55-37-680',
'03_Ball_Bearing_MR106ZZ_6x10x3',#11508,#11491);
#11508=PRODUCT_DEFINITION_FORMATION('',$,#11537);
#11532=APPLICATION_CONTEXT(
'Core Data for Automotive Mechanical Design Process');
#11533=PRODUCT_CONTEXT('part definition',#11532,'mechanical');
#11537=PRODUCT('2026-10-25-00-55-37-680',
'03_Ball_Bearing_MR106ZZ_6x10x3',$,(#11533));
#11603=COLOUR_RGB('Grey',0.48,0.52,0.57);
#11604=FILL_AREA_STYLE_COLOUR('',#11603);
#11605=FILL_AREA_STYLE('',(#11604));
#11606=SURFACE_STYLE_FILL_AREA(#11605);
#11607=SURFACE_SIDE_STYLE('',(#11606));
#11608=SURFACE_STYLE_USAGE(.BOTH.,#11607);
#11609=PRESENTATION_STYLE_ASSIGNMENT((#11608));
ENDSEC;
END-ISO-10303-21;
